ISO-10303-21;
HEADER;
/* Generated by software containing ST-Developer
 * from STEP Tools, Inc. (www.steptools.com) 
 */

FILE_DESCRIPTION(
/* description */ ('Hand-crank gear train demonstrator'),
/* implementation_level */ '2;1');

FILE_NAME(
/* name */ 'M4x10 Cap Screw.step',
/* time_stamp */ '2026-10-28T03:22:13-07:00',
/* author */ (''),
/* organization */ (''),
/* preprocessor_version */ 'ST-DEVELOPER v20.2',
/* originating_system */ 'Autodesk Translation Framework v15.17.0.0',
/* authorisation */ '');

FILE_SCHEMA (('AUTOMOTIVE_DESIGN { 1 0 10303 214 3 1 1 }'));
ENDSEC;

DATA;
#10=MECHANICAL_DESIGN_GEOMETRIC_PRESENTATION_REPRESENTATION('',(#1225),#62758);
#1036=CONICAL_SURFACE('',#17759,0.325,0.785398163397448);
#1037=CONICAL_SURFACE('',#17763,0.335,0.785398163397448);
#1038=CONICAL_SURFACE('',#17767,0.21,0.463647609000806);
#1052=ORIENTED_CLOSED_SHELL('',*,#16406,.F.);
#1057=BREP_WITH_VOIDS('Body1',#16407,(#1052));
#1082=SHAPE_REPRESENTATION_RELATIONSHIP('SRR','None',#63056,#1146);
#1146=ADVANCED_BREP_SHAPE_REPRESENTATION('',(#1057),#62710);
#1225=STYLED_ITEM('',(#63469),#1057);
#1505=FACE_BOUND('',#3473,.T.);
#1715=PLANE('',#17747);
#1716=PLANE('',#17748);
#1717=PLANE('',#17749);
#1718=PLANE('',#17750);
#1719=PLANE('',#17751);
#1720=PLANE('',#17752);
#1721=PLANE('',#17753);
#1722=PLANE('',#17754);
#1723=PLANE('',#17755);
#1724=PLANE('',#17757);
#1725=PLANE('',#17765);
#2360=FACE_OUTER_BOUND('',#3459,.T.);
#2361=FACE_OUTER_BOUND('',#3460,.T.);
#2362=FACE_OUTER_BOUND('',#3461,.T.);
#2363=FACE_OUTER_BOUND('',#3462,.T.);
#2364=FACE_OUTER_BOUND('',#3463,.T.);
#2365=FACE_OUTER_BOUND('',#3464,.T.);
#2366=FACE_OUTER_BOUND('',#3465,.T.);
#2367=FACE_OUTER_BOUND('',#3466,.T.);
#2368=FACE_OUTER_BOUND('',#3467,.T.);
#2369=FACE_OUTER_BOUND('',#3468,.T.);
#2370=FACE_OUTER_BOUND('',#3469,.T.);
#2371=FACE_OUTER_BOUND('',#3470,.T.);
#2372=FACE_OUTER_BOUND('',#3471,.T.);
#2373=FACE_OUTER_BOUND('',#3472,.T.);
#2374=FACE_OUTER_BOUND('',#3474,.T.);
#2375=FACE_OUTER_BOUND('',#3475,.T.);
#3459=EDGE_LOOP('',(#11869,#11870,#11871,#11872));
#3460=EDGE_LOOP('',(#11873,#11874,#11875,#11876));
#3461=EDGE_LOOP('',(#11877,#11878,#11879,#11880));
#3462=EDGE_LOOP('',(#11881,#11882,#11883,#11884));
#3463=EDGE_LOOP('',(#11885,#11886,#11887,#11888));
#3464=EDGE_LOOP('',(#11889,#11890,#11891,#11892));
#3465=EDGE_LOOP('',(#11893,#11894,#11895,#11896,#11897,#11898));
#3466=EDGE_LOOP('',(#11899,#11900,#11901,#11902,#11903,#11904));
#3467=EDGE_LOOP('',(#11905));
#3468=EDGE_LOOP('',(#11906));
#3469=EDGE_LOOP('',(#11907,#11908,#11909,#11910));
#3470=EDGE_LOOP('',(#11911,#11912,#11913,#11914));
#3471=EDGE_LOOP('',(#11915,#11916,#11917,#11918));
#3472=EDGE_LOOP('',(#11919));
#3473=EDGE_LOOP('',(#11920));
#3474=EDGE_LOOP('',(#11921,#11922,#11923,#11924));
#3475=EDGE_LOOP('',(#11925,#11926,#11927,#11928));
#4455=LINE('',#25095,#5587);
#4456=LINE('',#25097,#5588);
#4457=LINE('',#25099,#5589);
#4458=LINE('',#25100,#5590);
#4459=LINE('',#25103,#5591);
#4460=LINE('',#25105,#5592);
#4461=LINE('',#25106,#5593);
#4462=LINE('',#25109,#5594);
#4463=LINE('',#25111,#5595);
#4464=LINE('',#25112,#5596);
#4465=LINE('',#25115,#5597);
#4466=LINE('',#25117,#5598);
#4467=LINE('',#25118,#5599);
#4468=LINE('',#25121,#5600);
#4469=LINE('',#25123,#5601);
#4470=LINE('',#25124,#5602);
#4471=LINE('',#25126,#5603);
#4472=LINE('',#25127,#5604);
#4473=LINE('',#25139,#5605);
#4474=LINE('',#25143,#5606);
#4475=LINE('',#25147,#5607);
#4476=LINE('',#25154,#5608);
#4477=LINE('',#25156,#5609);
#5587=VECTOR('',#20180,1.);
#5588=VECTOR('',#20181,1.);
#5589=VECTOR('',#20182,1.);
#5590=VECTOR('',#20183,1.);
#5591=VECTOR('',#20186,1.);
#5592=VECTOR('',#20187,1.);
#5593=VECTOR('',#20188,1.);
#5594=VECTOR('',#20191,1.);
#5595=VECTOR('',#20192,1.);
#5596=VECTOR('',#20193,1.);
#5597=VECTOR('',#20196,1.);
#5598=VECTOR('',#20197,1.);
#5599=VECTOR('',#20198,1.);
#5600=VECTOR('',#20201,1.);
#5601=VECTOR('',#20202,1.);
#5602=VECTOR('',#20203,1.);
#5603=VECTOR('',#20206,1.);
#5604=VECTOR('',#20207,1.);
#5605=VECTOR('',#20224,0.325);
#5606=VECTOR('',#20229,0.35);
#5607=VECTOR('',#20234,0.335);
#5608=VECTOR('',#20243,0.21);
#5609=VECTOR('',#20246,0.2);
#6866=CIRCLE('',#17756,0.1954);
#6867=CIRCLE('',#17758,0.3);
#6868=CIRCLE('',#17760,0.35);
#6869=CIRCLE('',#17762,0.35);
#6870=CIRCLE('',#17764,0.32);
#6871=CIRCLE('',#17766,0.22);
#6872=CIRCLE('',#17768,0.1954);
#7573=VERTEX_POINT('',#25093);
#7574=VERTEX_POINT('',#25094);
#7575=VERTEX_POINT('',#25096);
#7576=VERTEX_POINT('',#25098);
#7577=VERTEX_POINT('',#25102);
#7578=VERTEX_POINT('',#25104);
#7579=VERTEX_POINT('',#25108);
#7580=VERTEX_POINT('',#25110);
#7581=VERTEX_POINT('',#25114);
#7582=VERTEX_POINT('',#25116);
#7583=VERTEX_POINT('',#25120);
#7584=VERTEX_POINT('',#25122);
#7585=VERTEX_POINT('',#25131);
#7586=VERTEX_POINT('',#25134);
#7587=VERTEX_POINT('',#25137);
#7588=VERTEX_POINT('',#25141);
#7589=VERTEX_POINT('',#25145);
#7590=VERTEX_POINT('',#25149);
#7591=VERTEX_POINT('',#25152);
#9186=EDGE_CURVE('',#7573,#7574,#4455,.T.);
#9187=EDGE_CURVE('',#7574,#7575,#4456,.T.);
#9188=EDGE_CURVE('',#7575,#7576,#4457,.T.);
#9189=EDGE_CURVE('',#7573,#7576,#4458,.T.);
#9190=EDGE_CURVE('',#7574,#7577,#4459,.T.);
#9191=EDGE_CURVE('',#7577,#7578,#4460,.T.);
#9192=EDGE_CURVE('',#7578,#7575,#4461,.T.);
#9193=EDGE_CURVE('',#7577,#7579,#4462,.T.);
#9194=EDGE_CURVE('',#7579,#7580,#4463,.T.);
#9195=EDGE_CURVE('',#7580,#7578,#4464,.T.);
#9196=EDGE_CURVE('',#7579,#7581,#4465,.T.);
#9197=EDGE_CURVE('',#7581,#7582,#4466,.T.);
#9198=EDGE_CURVE('',#7582,#7580,#4467,.T.);
#9199=EDGE_CURVE('',#7581,#7583,#4468,.T.);
#9200=EDGE_CURVE('',#7583,#7584,#4469,.T.);
#9201=EDGE_CURVE('',#7584,#7582,#4470,.T.);
#9202=EDGE_CURVE('',#7583,#7573,#4471,.T.);
#9203=EDGE_CURVE('',#7576,#7584,#4472,.T.);
#9204=EDGE_CURVE('',#7585,#7585,#6866,.T.);
#9205=EDGE_CURVE('',#7586,#7586,#6867,.T.);
#9206=EDGE_CURVE('',#7587,#7587,#6868,.T.);
#9207=EDGE_CURVE('',#7587,#7586,#4473,.T.);
#9208=EDGE_CURVE('',#7588,#7588,#6869,.T.);
#9209=EDGE_CURVE('',#7588,#7587,#4474,.T.);
#9210=EDGE_CURVE('',#7589,#7589,#6870,.T.);
#9211=EDGE_CURVE('',#7589,#7588,#4475,.T.);
#9212=EDGE_CURVE('',#7590,#7590,#6871,.T.);
#9213=EDGE_CURVE('',#7591,#7591,#6872,.F.);
#9214=EDGE_CURVE('',#7591,#7590,#4476,.T.);
#9215=EDGE_CURVE('',#7585,#7591,#4477,.T.);
#11869=ORIENTED_EDGE('',*,*,#9186,.T.);
#11870=ORIENTED_EDGE('',*,*,#9187,.T.);
#11871=ORIENTED_EDGE('',*,*,#9188,.T.);
#11872=ORIENTED_EDGE('',*,*,#9189,.F.);
#11873=ORIENTED_EDGE('',*,*,#9190,.T.);
#11874=ORIENTED_EDGE('',*,*,#9191,.T.);
#11875=ORIENTED_EDGE('',*,*,#9192,.T.);
#11876=ORIENTED_EDGE('',*,*,#9187,.F.);
#11877=ORIENTED_EDGE('',*,*,#9193,.T.);
#11878=ORIENTED_EDGE('',*,*,#9194,.T.);
#11879=ORIENTED_EDGE('',*,*,#9195,.T.);
#11880=ORIENTED_EDGE('',*,*,#9191,.F.);
#11881=ORIENTED_EDGE('',*,*,#9196,.T.);
#11882=ORIENTED_EDGE('',*,*,#9197,.T.);
#11883=ORIENTED_EDGE('',*,*,#9198,.T.);
#11884=ORIENTED_EDGE('',*,*,#9194,.F.);
#11885=ORIENTED_EDGE('',*,*,#9199,.T.);
#11886=ORIENTED_EDGE('',*,*,#9200,.T.);
#11887=ORIENTED_EDGE('',*,*,#9201,.T.);
#11888=ORIENTED_EDGE('',*,*,#9197,.F.);
#11889=ORIENTED_EDGE('',*,*,#9202,.T.);
#11890=ORIENTED_EDGE('',*,*,#9189,.T.);
#11891=ORIENTED_EDGE('',*,*,#9203,.T.);
#11892=ORIENTED_EDGE('',*,*,#9200,.F.);
#11893=ORIENTED_EDGE('',*,*,#9202,.F.);
#11894=ORIENTED_EDGE('',*,*,#9199,.F.);
#11895=ORIENTED_EDGE('',*,*,#9196,.F.);
#11896=ORIENTED_EDGE('',*,*,#9193,.F.);
#11897=ORIENTED_EDGE('',*,*,#9190,.F.);
#11898=ORIENTED_EDGE('',*,*,#9186,.F.);
#11899=ORIENTED_EDGE('',*,*,#9203,.F.);
#11900=ORIENTED_EDGE('',*,*,#9188,.F.);
#11901=ORIENTED_EDGE('',*,*,#9192,.F.);
#11902=ORIENTED_EDGE('',*,*,#9195,.F.);
#11903=ORIENTED_EDGE('',*,*,#9198,.F.);
#11904=ORIENTED_EDGE('',*,*,#9201,.F.);
#11905=ORIENTED_EDGE('',*,*,#9204,.F.);
#11906=ORIENTED_EDGE('',*,*,#9205,.F.);
#11907=ORIENTED_EDGE('',*,*,#9206,.F.);
#11908=ORIENTED_EDGE('',*,*,#9207,.T.);
#11909=ORIENTED_EDGE('',*,*,#9205,.T.);
#11910=ORIENTED_EDGE('',*,*,#9207,.F.);
#11911=ORIENTED_EDGE('',*,*,#9208,.F.);
#11912=ORIENTED_EDGE('',*,*,#9209,.T.);
#11913=ORIENTED_EDGE('',*,*,#9206,.T.);
#11914=ORIENTED_EDGE('',*,*,#9209,.F.);
#11915=ORIENTED_EDGE('',*,*,#9210,.F.);
#11916=ORIENTED_EDGE('',*,*,#9211,.T.);
#11917=ORIENTED_EDGE('',*,*,#9208,.T.);
#11918=ORIENTED_EDGE('',*,*,#9211,.F.);
#11919=ORIENTED_EDGE('',*,*,#9210,.T.);
#11920=ORIENTED_EDGE('',*,*,#9212,.F.);
#11921=ORIENTED_EDGE('',*,*,#9213,.F.);
#11922=ORIENTED_EDGE('',*,*,#9214,.T.);
#11923=ORIENTED_EDGE('',*,*,#9212,.T.);
#11924=ORIENTED_EDGE('',*,*,#9214,.F.);
#11925=ORIENTED_EDGE('',*,*,#9204,.T.);
#11926=ORIENTED_EDGE('',*,*,#9215,.T.);
#11927=ORIENTED_EDGE('',*,*,#9213,.T.);
#11928=ORIENTED_EDGE('',*,*,#9215,.F.);
#15277=CYLINDRICAL_SURFACE('',#17761,0.35);
#15278=CYLINDRICAL_SURFACE('',#17769,0.1954);
#15670=ADVANCED_FACE('',(#2360),#1715,.F.);
#15671=ADVANCED_FACE('',(#2361),#1716,.F.);
#15672=ADVANCED_FACE('',(#2362),#1717,.F.);
#15673=ADVANCED_FACE('',(#2363),#1718,.F.);
#15674=ADVANCED_FACE('',(#2364),#1719,.F.);
#15675=ADVANCED_FACE('',(#2365),#1720,.F.);
#15676=ADVANCED_FACE('',(#2366),#1721,.F.);
#15677=ADVANCED_FACE('',(#2367),#1722,.F.);
#15678=ADVANCED_FACE('',(#2368),#1723,.F.);
#15679=ADVANCED_FACE('',(#2369),#1724,.T.);
#15680=ADVANCED_FACE('',(#2370),#1036,.T.);
#15681=ADVANCED_FACE('',(#2371),#15277,.T.);
#15682=ADVANCED_FACE('',(#2372),#1037,.T.);
#15683=ADVANCED_FACE('',(#2373,#1505),#1725,.T.);
#15684=ADVANCED_FACE('',(#2374),#1038,.T.);
#15685=ADVANCED_FACE('',(#2375),#15278,.T.);
#16406=CLOSED_SHELL('',(#15670,#15671,#15672,#15673,#15674,#15675,#15676,
#15677));
#16407=CLOSED_SHELL('',(#15678,#15679,#15680,#15681,#15682,#15683,#15684,
#15685));
#17746=AXIS2_PLACEMENT_3D('',#25091,#20176,#20177);
#17747=AXIS2_PLACEMENT_3D('',#25092,#20178,#20179);
#17748=AXIS2_PLACEMENT_3D('',#25101,#20184,#20185);
#17749=AXIS2_PLACEMENT_3D('',#25107,#20189,#20190);
#17750=AXIS2_PLACEMENT_3D('',#25113,#20194,#20195);
#17751=AXIS2_PLACEMENT_3D('',#25119,#20199,#20200);
#17752=AXIS2_PLACEMENT_3D('',#25125,#20204,#20205);
#17753=AXIS2_PLACEMENT_3D('',#25128,#20208,#20209);
#17754=AXIS2_PLACEMENT_3D('',#25129,#20210,#20211);
#17755=AXIS2_PLACEMENT_3D('',#25130,#20212,#20213);
#17756=AXIS2_PLACEMENT_3D('',#25132,#20214,#20215);
#17757=AXIS2_PLACEMENT_3D('',#25133,#20216,#20217);
#17758=AXIS2_PLACEMENT_3D('',#25135,#20218,#20219);
#17759=AXIS2_PLACEMENT_3D('',#25136,#20220,#20221);
#17760=AXIS2_PLACEMENT_3D('',#25138,#20222,#20223);
#17761=AXIS2_PLACEMENT_3D('',#25140,#20225,#20226);
#17762=AXIS2_PLACEMENT_3D('',#25142,#20227,#20228);
#17763=AXIS2_PLACEMENT_3D('',#25144,#20230,#20231);
#17764=AXIS2_PLACEMENT_3D('',#25146,#20232,#20233);
#17765=AXIS2_PLACEMENT_3D('',#25148,#20235,#20236);
#17766=AXIS2_PLACEMENT_3D('',#25150,#20237,#20238);
#17767=AXIS2_PLACEMENT_3D('',#25151,#20239,#20240);
#17768=AXIS2_PLACEMENT_3D('',#25153,#20241,#20242);
#17769=AXIS2_PLACEMENT_3D('',#25155,#20244,#20245);
#20176=DIRECTION('axis',(0.,0.,1.));
#20177=DIRECTION('refdir',(1.,0.,0.));
#20178=DIRECTION('center_axis',(0.866025403784439,0.,-0.5));
#20179=DIRECTION('ref_axis',(0.5,0.,0.866025403784439));
#20180=DIRECTION('',(-0.5,0.,-0.866025403784439));
#20181=DIRECTION('',(0.,-1.,0.));
#20182=DIRECTION('',(0.5,0.,0.866025403784439));
#20183=DIRECTION('',(0.,-1.,0.));
#20184=DIRECTION('center_axis',(1.60246890531964E-16,0.,-1.));
#20185=DIRECTION('ref_axis',(1.,0.,1.60246890531964E-16));
#20186=DIRECTION('',(-1.,0.,-1.60246890531964E-16));
#20187=DIRECTION('',(0.,-1.,0.));
#20188=DIRECTION('',(1.,0.,1.60246890531964E-16));
#20189=DIRECTION('center_axis',(-0.866025403784439,0.,-0.5));
#20190=DIRECTION('ref_axis',(0.5,0.,-0.866025403784439));
#20191=DIRECTION('',(-0.5,0.,0.866025403784439));
#20192=DIRECTION('',(0.,-1.,0.));
#20193=DIRECTION('',(0.5,0.,-0.866025403784439));
#20194=DIRECTION('center_axis',(-0.866025403784439,0.,0.5));
#20195=DIRECTION('ref_axis',(-0.5,0.,-0.866025403784439));
#20196=DIRECTION('',(0.5,0.,0.866025403784439));
#20197=DIRECTION('',(0.,-1.,0.));
#20198=DIRECTION('',(-0.5,0.,-0.866025403784439));
#20199=DIRECTION('center_axis',(-1.60246890531964E-16,0.,1.));
#20200=DIRECTION('ref_axis',(-1.,0.,-1.60246890531964E-16));
#20201=DIRECTION('',(1.,0.,1.60246890531964E-16));
#20202=DIRECTION('',(0.,-1.,0.));
#20203=DIRECTION('',(-1.,0.,-1.60246890531964E-16));
#20204=DIRECTION('center_axis',(0.866025403784439,0.,0.5));
#20205=DIRECTION('ref_axis',(-0.5,0.,0.866025403784439));
#20206=DIRECTION('',(0.5,0.,-0.866025403784439));
#20207=DIRECTION('',(-0.5,0.,0.866025403784439));
#20208=DIRECTION('center_axis',(0.,1.,0.));
#20209=DIRECTION('ref_axis',(1.,0.,0.));
#20210=DIRECTION('center_axis',(0.,-1.,0.));
#20211=DIRECTION('ref_axis',(0.,0.,-1.));
#20212=DIRECTION('center_axis',(0.,1.,0.));
#20213=DIRECTION('ref_axis',(1.,0.,0.));
#20214=DIRECTION('center_axis',(0.,1.,0.));
#20215=DIRECTION('ref_axis',(1.,0.,0.));
#20216=DIRECTION('center_axis',(0.,1.,0.));
#20217=DIRECTION('ref_axis',(0.,0.,1.));
#20218=DIRECTION('center_axis',(0.,-1.,0.));
#20219=DIRECTION('ref_axis',(1.,0.,0.));
#20220=DIRECTION('center_axis',(0.,-1.,0.));
#20221=DIRECTION('ref_axis',(1.,0.,0.));
#20222=DIRECTION('center_axis',(0.,-1.,0.));
#20223=DIRECTION('ref_axis',(1.,0.,0.));
#20224=DIRECTION('',(0.707106781186547,0.707106781186548,8.65956056235493E-17));
#20225=DIRECTION('center_axis',(0.,-1.,0.));
#20226=DIRECTION('ref_axis',(1.,0.,0.));
#20227=DIRECTION('center_axis',(0.,-1.,0.));
#20228=DIRECTION('ref_axis',(1.,0.,0.));
#20229=DIRECTION('',(0.,1.,0.));
#20230=DIRECTION('center_axis',(0.,1.,0.));
#20231=DIRECTION('ref_axis',(1.,0.,0.));
#20232=DIRECTION('center_axis',(0.,-1.,0.));
#20233=DIRECTION('ref_axis',(1.,0.,0.));
#20234=DIRECTION('',(-0.707106781186547,0.707106781186548,-8.65956056235493E-17));
#20235=DIRECTION('center_axis',(0.,-1.,0.));
#20236=DIRECTION('ref_axis',(0.,0.,-1.));
#20237=DIRECTION('center_axis',(0.,-1.,0.));
#20238=DIRECTION('ref_axis',(1.,0.,0.));
#20239=DIRECTION('center_axis',(0.,1.,0.));
#20240=DIRECTION('ref_axis',(1.,0.,0.));
#20241=DIRECTION('center_axis',(0.,1.,0.));
#20242=DIRECTION('ref_axis',(1.,0.,0.));
#20243=DIRECTION('',(-0.447213595499958,0.894427190999916,-5.47678698264203E-17));
#20244=DIRECTION('center_axis',(0.,-1.,0.));
#20245=DIRECTION('ref_axis',(1.,0.,0.));
#20246=DIRECTION('',(0.,1.,0.));
#25091=CARTESIAN_POINT('',(0.,0.,0.));
#25092=CARTESIAN_POINT('Origin',(0.0866025403784439,-0.4,-0.15));
#25093=CARTESIAN_POINT('',(0.173205080756888,-0.4,0.));
#25094=CARTESIAN_POINT('',(0.0866025403784439,-0.4,-0.15));
#25095=CARTESIAN_POINT('',(0.173205080756888,-0.4,0.));
#25096=CARTESIAN_POINT('',(0.0866025403784439,-0.64,-0.15));
#25097=CARTESIAN_POINT('',(0.0866025403784439,-0.4,-0.15));
#25098=CARTESIAN_POINT('',(0.173205080756888,-0.64,0.));
#25099=CARTESIAN_POINT('',(0.173205080756888,-0.64,0.));
#25100=CARTESIAN_POINT('',(0.173205080756888,-0.4,0.));
#25101=CARTESIAN_POINT('Origin',(-0.0866025403784438,-0.4,-0.15));
#25102=CARTESIAN_POINT('',(-0.0866025403784438,-0.4,-0.15));
#25103=CARTESIAN_POINT('',(0.0866025403784439,-0.4,-0.15));
#25104=CARTESIAN_POINT('',(-0.0866025403784438,-0.64,-0.15));
#25105=CARTESIAN_POINT('',(-0.0866025403784438,-0.4,-0.15));
#25106=CARTESIAN_POINT('',(0.0866025403784439,-0.64,-0.15));
#25107=CARTESIAN_POINT('Origin',(-0.173205080756888,-0.4,-2.77555756156289E-17));
#25108=CARTESIAN_POINT('',(-0.173205080756888,-0.4,-2.12115047744981E-17));
#25109=CARTESIAN_POINT('',(-0.0866025403784438,-0.4,-0.15));
#25110=CARTESIAN_POINT('',(-0.173205080756888,-0.64,-2.77555756156289E-17));
#25111=CARTESIAN_POINT('',(-0.173205080756888,-0.4,-2.12115047744981E-17));
#25112=CARTESIAN_POINT('',(-0.0866025403784438,-0.64,-0.15));
#25113=CARTESIAN_POINT('Origin',(-0.0866025403784439,-0.4,0.15));
#25114=CARTESIAN_POINT('',(-0.0866025403784439,-0.4,0.15));
#25115=CARTESIAN_POINT('',(-0.173205080756888,-0.4,-2.12115047744981E-17));
#25116=CARTESIAN_POINT('',(-0.0866025403784439,-0.64,0.15));
#25117=CARTESIAN_POINT('',(-0.0866025403784439,-0.4,0.15));
#25118=CARTESIAN_POINT('',(-0.173205080756888,-0.64,-2.12115047744981E-17));
#25119=CARTESIAN_POINT('Origin',(0.0866025403784439,-0.4,0.15));
#25120=CARTESIAN_POINT('',(0.0866025403784439,-0.4,0.15));
#25121=CARTESIAN_POINT('',(-0.0866025403784439,-0.4,0.15));
#25122=CARTESIAN_POINT('',(0.0866025403784439,-0.64,0.15));
#25123=CARTESIAN_POINT('',(0.0866025403784439,-0.4,0.15));
#25124=CARTESIAN_POINT('',(-0.0866025403784439,-0.64,0.15));
#25125=CARTESIAN_POINT('Origin',(0.173205080756888,-0.4,0.));
#25126=CARTESIAN_POINT('',(0.0866025403784439,-0.4,0.15));
#25127=CARTESIAN_POINT('',(0.0866025403784439,-0.64,0.15));
#25128=CARTESIAN_POINT('Origin',(0.,-0.4,-2.77555756156289E-17));
#25129=CARTESIAN_POINT('Origin',(0.,-0.64,-2.77555756156289E-17));
#25130=CARTESIAN_POINT('Origin',(0.,-1.,0.));
#25131=CARTESIAN_POINT('',(-0.1954,-1.,2.39295984553393E-17));
#25132=CARTESIAN_POINT('Origin',(0.,-1.,0.));
#25133=CARTESIAN_POINT('Origin',(0.3,0.4,0.));
#25134=CARTESIAN_POINT('',(-0.3,0.4,-3.67394039744206E-17));
#25135=CARTESIAN_POINT('Origin',(0.,0.4,0.));
#25136=CARTESIAN_POINT('Origin',(0.,0.375,0.));
#25137=CARTESIAN_POINT('',(-0.35,0.35,-4.28626379701573E-17));
#25138=CARTESIAN_POINT('Origin',(0.,0.35,0.));
#25139=CARTESIAN_POINT('',(-0.325,0.375,-3.9801020972289E-17));
#25140=CARTESIAN_POINT('Origin',(0.,0.19,0.));
#25141=CARTESIAN_POINT('',(-0.35,0.03,-4.28626379701574E-17));
#25142=CARTESIAN_POINT('Origin',(0.,0.03,0.));
#25143=CARTESIAN_POINT('',(-0.35,0.19,-4.28626379701574E-17));
#25144=CARTESIAN_POINT('Origin',(0.,0.0149999999999999,0.));
#25145=CARTESIAN_POINT('',(-0.32,-3.29597460435593E-17,-3.91886975727153E-17));
#25146=CARTESIAN_POINT('Origin',(0.,0.,0.));
#25147=CARTESIAN_POINT('',(-0.335,0.0149999999999999,-4.10256677714363E-17));
#25148=CARTESIAN_POINT('Origin',(0.22,0.,0.));
#25149=CARTESIAN_POINT('',(-0.22,-6.93889390390723E-18,-2.69422295812418E-17));
#25150=CARTESIAN_POINT('Origin',(0.,0.,0.));
#25151=CARTESIAN_POINT('Origin',(0.,-0.02,0.));
#25152=CARTESIAN_POINT('',(-0.1954,-0.0492,2.39295984553393E-17));
#25153=CARTESIAN_POINT('Origin',(0.,-0.0492,0.));
#25154=CARTESIAN_POINT('',(-0.21,-0.02,-2.57175827820944E-17));
#25155=CARTESIAN_POINT('Origin',(0.,-0.8,0.));
#25156=CARTESIAN_POINT('',(-0.1954,-0.8,-2.39295984553393E-17));
#62636=UNCERTAINTY_MEASURE_WITH_UNIT(LENGTH_MEASURE(0.001),#62759,
'DISTANCE_ACCURACY_VALUE',
'Maximum model space distance between geometric entities at asserted c
onnectivities');
#62684=UNCERTAINTY_MEASURE_WITH_UNIT(LENGTH_MEASURE(0.001),#62759,
'DISTANCE_ACCURACY_VALUE',
'Maximum model space distance between geometric entities at asserted c
onnectivities');
#62710=(
GEOMETRIC_REPRESENTATION_CONTEXT(3)
GLOBAL_UNCERTAINTY_ASSIGNED_CONTEXT((#62636))
GLOBAL_UNIT_ASSIGNED_CONTEXT((#62759,#62761,#62762))
REPRESENTATION_CONTEXT('','3D')
);
#62758=(
GEOMETRIC_REPRESENTATION_CONTEXT(3)
GLOBAL_UNCERTAINTY_ASSIGNED_CONTEXT((#62684))
GLOBAL_UNIT_ASSIGNED_CONTEXT((#62759,#62761,#62762))
REPRESENTATION_CONTEXT('','3D')
);
#62759=(
LENGTH_UNIT()
NAMED_UNIT(*)
SI_UNIT(.CENTI.,.METRE.)
);
#62761=(
NAMED_UNIT(*)
PLANE_ANGLE_UNIT()
SI_UNIT($,.RADIAN.)
);
#62762=(
NAMED_UNIT(*)
SI_UNIT($,.STERADIAN.)
SOLID_ANGLE_UNIT()
);
#62788=SHAPE_DEFINITION_REPRESENTATION(#62871,#63056);
#62871=PRODUCT_DEFINITION_SHAPE('',$,#63130);
#63056=SHAPE_REPRESENTATION('',(#17746),#62710);
#63104=PRODUCT_DEFINITION_CONTEXT('part definition',#63325,'design');
#63130=PRODUCT_DEFINITION('M4x10 Cap Screw','M4x10 Cap Screw',#63203,#63104);
#63203=PRODUCT_DEFINITION_FORMATION('',$,#63352);
#63325=APPLICATION_CONTEXT(
'Core Data for Automotive Mechanical Design Process');
#63326=PRODUCT_CONTEXT('part definition',#63325,'mechanical');
#63352=PRODUCT('M4x10 Cap Screw','M4x10 Cap Screw','M4x10 Cap Screw',(#63326));
#63463=COLOUR_RGB('Black',0.12,0.14,0.17);
#63464=FILL_AREA_STYLE_COLOUR('',#63463);
#63465=FILL_AREA_STYLE('',(#63464));
#63466=SURFACE_STYLE_FILL_AREA(#63465);
#63467=SURFACE_SIDE_STYLE('',(#63466));
#63468=SURFACE_STYLE_USAGE(.BOTH.,#63467);
#63469=PRESENTATION_STYLE_ASSIGNMENT((#63468));
ENDSEC;
END-ISO-10303-21;
